ISO-10303-21;
HEADER;
FILE_DESCRIPTION (('STEP AP214'),
    '1' );
FILE_NAME ('circlip for shafts normal_din_Circlip DIN 471 - 10 x 1.step',
    '2026-10-24T07:08:27',
    ( '' ),
    ( '' ),
    'SwSTEP 2.0',
    'SolidWorks 2026',
    '' );
FILE_SCHEMA (( 'AUTOMOTIVE_DESIGN' ));
ENDSEC;

DATA;
#3=EDGE_CURVE ( 'NONE', #2619, #17682, #10723, .T. ) ;
#69=PLANE ( 'NONE',  #12942 ) ;
#116=CARTESIAN_POINT ( 'NONE',  ( -3.098410542199071749, -7.060458129626440815, 0.000000000000000000 ) ) ;
#152=DIRECTION ( 'NONE',  ( -0.000000000000000000, -0.000000000000000000, -1.000000000000000000 ) ) ;
#161=ORIENTED_EDGE ( 'NONE', *, *, #10210, .F. ) ;
#168=VERTEX_POINT ( 'NONE', #13239 ) ;
#176=AXIS2_PLACEMENT_3D ( 'NONE', #3253, #211, #16295 ) ;
#211=DIRECTION ( 'NONE',  ( 0.000000000000000000, 0.000000000000000000, 1.000000000000000000 ) ) ;
#217=CARTESIAN_POINT ( 'NONE',  ( -2.354826896168714434, -6.962563485461402024, 0.000000000000000000 ) ) ;
#221=PRODUCT_CONTEXT ( 'NONE', #9864, 'mechanical' ) ;
#255=LINE ( 'NONE', #14921, #9366 ) ;
#276=VERTEX_POINT ( 'NONE', #6560 ) ;
#287=ORIENTED_EDGE ( 'NONE', *, *, #9710, .T. ) ;
#299=CARTESIAN_POINT ( 'NONE',  ( 0.5000000000000000000, -6.429618962271402616, -1.000000000000000000 ) ) ;
#317=ORIENTED_EDGE ( 'NONE', *, *, #10109, .T. ) ;
#346=EDGE_LOOP ( 'NONE', ( #14600, #18802, #11785, #7106 ) ) ;
#350=ORIENTED_EDGE ( 'NONE', *, *, #9102, .F. ) ;
#351=DIRECTION ( 'NONE',  ( 0.000000000000000000, 0.000000000000000000, 1.000000000000000000 ) ) ;
#391=DIRECTION ( 'NONE',  ( 1.000000000000000000, 0.000000000000000000, 0.000000000000000000 ) ) ;
#392=ORIENTED_EDGE ( 'NONE', *, *, #3, .F. ) ;
#393=DIRECTION ( 'NONE',  ( 0.000000000000000000, 0.000000000000000000, 1.000000000000000000 ) ) ;
#430=DIRECTION ( 'NONE',  ( 1.000000000000000000, 0.000000000000000000, 0.000000000000000000 ) ) ;
#434=SHAPE_REPRESENTATION ( 'circlip for shafts normal_din_Circlip DIN 471 - 10 x 1', ( #8017 ), #1061 ) ;
#435=VERTEX_POINT ( 'NONE', #5522 ) ;
#444=FILL_AREA_STYLE ('',( #9397 ) ) ;
#494=AXIS2_PLACEMENT_3D ( 'NONE', #9814, #2390, #9620 ) ;
#532=CARTESIAN_POINT ( 'NONE',  ( -3.309651814758565180, -5.455921364805393026, 0.000000000000000000 ) ) ;
#609=ORIENTED_EDGE ( 'NONE', *, *, #12136, .F. ) ;
#686=EDGE_CURVE ( 'NONE', #12093, #4981, #3289, .T. ) ;
#700=FACE_OUTER_BOUND ( 'NONE', #13011, .T. ) ;
#704=EDGE_CURVE ( 'NONE', #7573, #2619, #14807, .T. ) ;
#708=FACE_BOUND ( 'NONE', #15504, .T. ) ;
#722=ORIENTED_EDGE ( 'NONE', *, *, #18740, .F. ) ;
#742=DIRECTION ( 'NONE',  ( -0.000000000000000000, -0.000000000000000000, -1.000000000000000000 ) ) ;
#806=VERTEX_POINT ( 'NONE', #6331 ) ;
#807=CIRCLE ( 'NONE', #9610, 6.080745460913608902 ) ;
#840=CIRCLE ( 'NONE', #16638, 2.396904916527699214 ) ;
#845=VERTEX_POINT ( 'NONE', #8239 ) ;
#853=ORIENTED_EDGE ( 'NONE', *, *, #2346, .T. ) ;
#881=DIRECTION ( 'NONE',  ( 0.000000000000000000, 0.000000000000000000, 1.000000000000000000 ) ) ;
#903=DIRECTION ( 'NONE',  ( 0.000000000000000000, 0.000000000000000000, 1.000000000000000000 ) ) ;
#907=DIRECTION ( 'NONE',  ( 1.000000000000000000, 0.000000000000000000, 0.000000000000000000 ) ) ;
#930=ORIENTED_EDGE ( 'NONE', *, *, #7358, .T. ) ;
#935=EDGE_CURVE ( 'NONE', #12093, #13795, #11151, .T. ) ;
#974=CARTESIAN_POINT ( 'NONE',  ( 2.000000000000000000, -6.429618962271402616, 0.000000000000000000 ) ) ;
#981=AXIS2_PLACEMENT_3D ( 'NONE', #2769, #16864, #12672 ) ;
#1038=DIRECTION ( 'NONE',  ( 0.000000000000000000, 0.000000000000000000, 1.000000000000000000 ) ) ;
#1043=CARTESIAN_POINT ( 'NONE',  ( 1.250000000000000000, -6.429618962271402616, -1.000000000000000000 ) ) ;
#1049=ORIENTED_EDGE ( 'NONE', *, *, #1352, .T. ) ;
#1061=( GEOMETRIC_REPRESENTATION_CONTEXT ( 3 ) GLOBAL_UNCERTAINTY_ASSIGNED_CONTEXT ( ( #11305 ) ) GLOBAL_UNIT_ASSIGNED_CONTEXT ( ( #18056, #3403, #7766 ) ) REPRESENTATION_CONTEXT ( 'NONE', 'WORKASPACE' ) );
#1062=DIRECTION ( 'NONE',  ( 1.000000000000000000, 0.000000000000000000, 0.000000000000000000 ) ) ;
#1166=DIRECTION ( 'NONE',  ( 0.000000000000000000, 0.000000000000000000, 1.000000000000000000 ) ) ;
#1205=EDGE_CURVE ( 'NONE', #18729, #276, #10244, .T. ) ;
#1210=ORIENTED_EDGE ( 'NONE', *, *, #9710, .F. ) ;
#1225=PRODUCT_DEFINITION_CONTEXT ( 'detailed design', #14726, 'design' ) ;
#1239=CARTESIAN_POINT ( 'NONE',  ( 0.2499999999999966416, -8.096141056083448362, 0.000000000000000000 ) ) ;
#1261=DIRECTION ( 'NONE',  ( -0.000000000000000000, -0.000000000000000000, -1.000000000000000000 ) ) ;
#1267=CIRCLE ( 'NONE', #12516, 2.396904916527700102 ) ;
#1281=CARTESIAN_POINT ( 'NONE',  ( -5.686050877451574337, -5.768780236673276995, -1.000000000000000000 ) ) ;
#1288=CARTESIAN_POINT ( 'NONE',  ( 0.000000000000000000, 0.5192545390863916310, 0.000000000000000000 ) ) ;
#1335=ORIENTED_EDGE ( 'NONE', *, *, #10484, .T. ) ;
#1336=DIRECTION ( 'NONE',  ( 0.000000000000000000, 0.000000000000000000, 1.000000000000000000 ) ) ;
#1352=EDGE_CURVE ( 'NONE', #7394, #3875, #6934, .T. ) ;
#1417=VECTOR ( 'NONE', #10306, 999.9999999999998863 ) ;
#1424=CARTESIAN_POINT ( 'NONE',  ( 0.000000000000000000, 0.000000000000000000, -1.000000000000000000 ) ) ;
#1464=DIRECTION ( 'NONE',  ( 0.000000000000000000, 0.000000000000000000, 1.000000000000000000 ) ) ;
#1474=CARTESIAN_POINT ( 'NONE',  ( 3.309651814758565180, -5.455921364805393026, -1.000000000000000000 ) ) ;
#1480=AXIS2_PLACEMENT_3D ( 'NONE', #15914, #11251, #1062 ) ;
#1489=VERTEX_POINT ( 'NONE', #4516 ) ;
#1580=DIRECTION ( 'NONE',  ( 0.000000000000000000, 0.000000000000000000, 1.000000000000000000 ) ) ;
#1582=ORIENTED_EDGE ( 'NONE', *, *, #15882, .F. ) ;
#1639=MECHANICAL_DESIGN_GEOMETRIC_PRESENTATION_REPRESENTATION('',(#5608),#8941);
#1642=CARTESIAN_POINT ( 'NONE',  ( -0.2500000000000000000, -8.096141056083446585, 0.000000000000000000 ) ) ;
#1665=EDGE_CURVE ( 'NONE', #1489, #15209, #9351, .T. ) ;
#1685=CIRCLE ( 'NONE', #18724, 4.799999999999999822 ) ;
#1754=ORIENTED_EDGE ( 'NONE', *, *, #3307, .T. ) ;
#1762=CARTESIAN_POINT ( 'NONE',  ( 4.078421086530217288, -3.990950201428958621, -1.000000000000000000 ) ) ;
#1763=CARTESIAN_POINT ( 'NONE',  ( 1.250000000000000000, -6.429618962271402616, -1.000000000000000000 ) ) ;
#1774=AXIS2_PLACEMENT_3D ( 'NONE', #18003, #10849, #14876 ) ;
#1804=DIRECTION ( 'NONE',  ( 0.000000000000000000, 0.000000000000000000, 1.000000000000000000 ) ) ;
#1815=CARTESIAN_POINT ( 'NONE',  ( -6.080745460913608902, 0.5192545390863924082, -1.000000000000000000 ) ) ;
#1826=VERTEX_POINT ( 'NONE', #15925 ) ;
#1834=ORIENTED_EDGE ( 'NONE', *, *, #14611, .F. ) ;
#1850=ORIENTED_EDGE ( 'NONE', *, *, #9763, .F. ) ;
#1871=VERTEX_POINT ( 'NONE', #2981 ) ;
#1887=DIRECTION ( 'NONE',  ( 0.000000000000000000, 0.000000000000000000, 1.000000000000000000 ) ) ;
#1918=EDGE_LOOP ( 'NONE', ( #392, #6607, #2504, #17630 ) ) ;
#1973=ORIENTED_EDGE ( 'NONE', *, *, #3716, .T. ) ;
#1979=DIRECTION ( 'NONE',  ( 0.000000000000000000, 0.000000000000000000, 1.000000000000000000 ) ) ;
#2005=EDGE_LOOP ( 'NONE', ( #7388, #9322, #8554, #8360 ) ) ;
#2030=ADVANCED_FACE ( 'NONE', ( #6390 ), #7533, .T. ) ;
#2061=ORIENTED_EDGE ( 'NONE', *, *, #17397, .F. ) ;
#2077=VECTOR ( 'NONE', #2768, 1000.000000000000000 ) ;
#2085=VERTEX_POINT ( 'NONE', #17916 ) ;
#2089=CARTESIAN_POINT ( 'NONE',  ( -1.250000000000000000, -6.429618962271402616, -1.000000000000000000 ) ) ;
#2116=ORIENTED_EDGE ( 'NONE', *, *, #11100, .F. ) ;
#2150=UNCERTAINTY_MEASURE_WITH_UNIT (LENGTH_MEASURE( 1.000000000000000082E-05 ), #3560, 'distance_accuracy_value', 'NONE');
#2154=EDGE_CURVE ( 'NONE', #17009, #7434, #11138, .T. ) ;
#2174=CARTESIAN_POINT ( 'NONE',  ( 2.595115354961440524, -7.673029147243177306, 0.000000000000000000 ) ) ;
#2179=DIRECTION ( 'NONE',  ( 0.000000000000000000, 0.000000000000000000, 1.000000000000000000 ) ) ;
#2220=FACE_OUTER_BOUND ( 'NONE', #5493, .T. ) ;
#2318=VECTOR ( 'NONE', #1804, 1000.000000000000000 ) ;
#2321=CARTESIAN_POINT ( 'NONE',  ( 2.595115354961440524, -7.673029147243177306, -1.000000000000000000 ) ) ;
#2324=CIRCLE ( 'NONE', #7192, 0.7500000000000000000 ) ;
#2346=EDGE_CURVE ( 'NONE', #806, #2539, #15905, .T. ) ;
#2358=CARTESIAN_POINT ( 'NONE',  ( 0.000000000000000000, 0.000000000000000000, -1.000000000000000000 ) ) ;
#2390=DIRECTION ( 'NONE',  ( 0.000000000000000000, 0.000000000000000000, 1.000000000000000000 ) ) ;
#2399=CIRCLE ( 'NONE', #12429, 0.7499999999999997780 ) ;
#2405=CARTESIAN_POINT ( 'NONE',  ( 3.309651814758565180, -5.455921364805393026, 0.000000000000000000 ) ) ;
#2419=LINE ( 'NONE', #9458, #14102 ) ;
#2483=EDGE_CURVE ( 'NONE', #4644, #1826, #6669, .T. ) ;
#2487=DIRECTION ( 'NONE',  ( 0.03086419753086420623, 0.9995235871707959241, -0.000000000000000000 ) ) ;
#2504=ORIENTED_EDGE ( 'NONE', *, *, #17397, .T. ) ;
#2513=AXIS2_PLACEMENT_3D ( 'NONE', #6551, #12358, #5124 ) ;
#2539=VERTEX_POINT ( 'NONE', #9131 ) ;
#2573=LINE ( 'NONE', #2867, #18208 ) ;
#2589=CARTESIAN_POINT ( 'NONE',  ( -5.686050877451574337, -5.768780236673276995, 0.000000000000000000 ) ) ;
#2606=EDGE_CURVE ( 'NONE', #15209, #1489, #10008, .T. ) ;
#2619=VERTEX_POINT ( 'NONE', #2174 ) ;
#2638=AXIS2_PLACEMENT_3D ( 'NONE', #14376, #1336, #17512 ) ;
#2666=PRODUCT ( 'circlip for shafts normal_din_Circlip DIN 471 - 10 x 1', 'circlip for shafts normal_din_Circlip DIN 471 - 10 x 1', '', ( #221 ) ) ;
#2668=CYLINDRICAL_SURFACE ( 'NONE', #2638, 6.080745460913608902 ) ;
#2682=VECTOR ( 'NONE', #17297, 1000.000000000000114 ) ;
#2743=UNCERTAINTY_MEASURE_WITH_UNIT (LENGTH_MEASURE( 1.000000000000000082E-05 ), #3690, 'distance_accuracy_value', 'NONE');
#2768=DIRECTION ( 'NONE',  ( 0.000000000000000000, 0.000000000000000000, 1.000000000000000000 ) ) ;
#2769=CARTESIAN_POINT ( 'NONE',  ( 2.354826896168714434, -6.962563485461402024, -1.000000000000000000 ) ) ;
#2784=VERTEX_POINT ( 'NONE', #8463 ) ;
#2788=DIRECTION ( 'NONE',  ( 0.000000000000000000, 0.000000000000000000, 1.000000000000000000 ) ) ;
#2851=ADVANCED_FACE ( 'NONE', ( #3397 ), #4828, .T. ) ;
#2867=CARTESIAN_POINT ( 'NONE',  ( -0.1481481481481481122, -4.797713218419819903, -1.000000000000000000 ) ) ;
#2880=ORIENTED_EDGE ( 'NONE', *, *, #16473, .F. ) ;
#2935=CIRCLE ( 'NONE', #494, 8.099999999999999645 ) ;
#2959=CARTESIAN_POINT ( 'NONE',  ( 3.098410542199072637, -7.060458129626440815, -1.000000000000000000 ) ) ;
#2981=CARTESIAN_POINT ( 'NONE',  ( -0.5000000000000000000, -6.429618962271402616, 0.000000000000000000 ) ) ;
#3020=FACE_OUTER_BOUND ( 'NONE', #10431, .T. ) ;
#3027=ORIENTED_EDGE ( 'NONE', *, *, #6680, .F. ) ;
#3063=LINE ( 'NONE', #15222, #3877 ) ;
#3064=CARTESIAN_POINT ( 'NONE',  ( -2.354826896168714434, -6.962563485461402024, -1.000000000000000000 ) ) ;
#3070=CIRCLE ( 'NONE', #5504, 8.099999999999999645 ) ;
#3096=LINE ( 'NONE', #3377, #18739 ) ;
#3157=CARTESIAN_POINT ( 'NONE',  ( -1.250000000000000000, -6.429618962271402616, 0.000000000000000000 ) ) ;
#3199=FACE_OUTER_BOUND ( 'NONE', #18198, .T. ) ;
#3225=DIRECTION ( 'NONE',  ( 0.000000000000000000, 0.000000000000000000, 1.000000000000000000 ) ) ;
#3253=CARTESIAN_POINT ( 'NONE',  ( 1.250000000000000000, -6.429618962271402616, 0.000000000000000000 ) ) ;
#3289=LINE ( 'NONE', #17576, #5759 ) ;
#3300=AXIS2_PLACEMENT_3D ( 'NONE', #217, #7541, #4679 ) ;
#3307=EDGE_CURVE ( 'NONE', #12824, #6434, #3096, .T. ) ;
#3340=ORIENTED_EDGE ( 'NONE', *, *, #5855, .F. ) ;
#3357=CARTESIAN_POINT ( 'NONE',  ( 1.250000000000000000, -6.429618962271402616, -1.000000000000000000 ) ) ;
#3369=DIRECTION ( 'NONE',  ( 0.000000000000000000, 0.000000000000000000, 1.000000000000000000 ) ) ;
#3377=CARTESIAN_POINT ( 'NONE',  ( -4.078421086530219064, -3.990950201428956845, -1.000000000000000000 ) ) ;
#3387=LINE ( 'NONE', #532, #4141 ) ;
#3397=FACE_OUTER_BOUND ( 'NONE', #1918, .T. ) ;
#3403=( NAMED_UNIT ( * ) PLANE_ANGLE_UNIT ( ) SI_UNIT ( $, .RADIAN. ) );
#3417=CARTESIAN_POINT ( 'NONE',  ( 0.000000000000000000, 0.5192545390863916310, -1.000000000000000000 ) ) ;
#3553=DIRECTION ( 'NONE',  ( 0.1305261922200524616, 0.9914448613738103822, -0.000000000000000000 ) ) ;
#3560=( LENGTH_UNIT ( ) NAMED_UNIT ( * ) SI_UNIT ( .MILLI., .METRE. ) );
#3567=FACE_OUTER_BOUND ( 'NONE', #4961, .T. ) ;
#3570=DIRECTION ( 'NONE',  ( 1.000000000000000000, 0.000000000000000000, 0.000000000000000000 ) ) ;
#3648=ORIENTED_EDGE ( 'NONE', *, *, #1205, .F. ) ;
#3658=DIRECTION ( 'NONE',  ( 0.1305261922200524338, 0.9914448613738102711, 0.000000000000000000 ) ) ;
#3690=( LENGTH_UNIT ( ) NAMED_UNIT ( * ) SI_UNIT ( .MILLI., .METRE. ) );
#3716=EDGE_CURVE ( 'NONE', #16631, #845, #2324, .T. ) ;
#3742=CARTESIAN_POINT ( 'NONE',  ( -1.250000000000000000, -6.429618962271402616, -1.000000000000000000 ) ) ;
#3812=AXIS2_PLACEMENT_3D ( 'NONE', #17545, #393, #4772 ) ;
#3875=VERTEX_POINT ( 'NONE', #1239 ) ;
#3877=VECTOR ( 'NONE', #10817, 1000.000000000000000 ) ;
#4083=DIRECTION ( 'NONE',  ( 1.000000000000000000, 0.000000000000000000, -0.000000000000000000 ) ) ;
#4090=ORIENTED_EDGE ( 'NONE', *, *, #10079, .F. ) ;
#4105=ORIENTED_EDGE ( 'NONE', *, *, #11525, .T. ) ;
#4141=VECTOR ( 'NONE', #4621, 999.9999999999998863 ) ;
#4167=CARTESIAN_POINT ( 'NONE',  ( 0.000000000000000000, 0.000000000000000000, -1.000000000000000000 ) ) ;
#4190=CIRCLE ( 'NONE', #6616, 0.7500000000000000000 ) ;
#4225=LINE ( 'NONE', #4496, #6137 ) ;
#4227=ADVANCED_BREP_SHAPE_REPRESENTATION ( '', ( #9242, #8017 ), #1061 ) ;
#4277=CARTESIAN_POINT ( 'NONE',  ( -0.1481481481481481122, -4.797713218419819903, -1.000000000000000000 ) ) ;
#4278=ORIENTED_EDGE ( 'NONE', *, *, #14611, .T. ) ;
#4305=EDGE_CURVE ( 'NONE', #4564, #9997, #14428, .T. ) ;
#4328=CARTESIAN_POINT ( 'NONE',  ( 0.1481481481481481122, -4.797713218419819903, 0.000000000000000000 ) ) ;
#4343=ADVANCED_FACE ( 'NONE', ( #18628 ), #7188, .F. ) ;
#4353=CARTESIAN_POINT ( 'NONE',  ( 0.000000000000000000, 0.000000000000000000, -1.000000000000000000 ) ) ;
#4406=ORIENTED_EDGE ( 'NONE', *, *, #8194, .T. ) ;
#4488=FACE_OUTER_BOUND ( 'NONE', #14426, .T. ) ;
#4496=CARTESIAN_POINT ( 'NONE',  ( -0.1481481481481481122, -4.797713218419819903, -1.000000000000000000 ) ) ;
#4516=CARTESIAN_POINT ( 'NONE',  ( -0.5000000000000000000, -6.429618962271402616, -1.000000000000000000 ) ) ;
#4535=CYLINDRICAL_SURFACE ( 'NONE', #8962, 0.7500000000000000000 ) ;
#4546=ORIENTED_EDGE ( 'NONE', *, *, #11100, .T. ) ;
#4564=VERTEX_POINT ( 'NONE', #18406 ) ;
#4587=ORIENTED_EDGE ( 'NONE', *, *, #9763, .T. ) ;
#4588=DIRECTION ( 'NONE',  ( 1.000000000000000000, 0.000000000000000000, 0.000000000000000000 ) ) ;
#4604=DIRECTION ( 'NONE',  ( 0.000000000000000000, 0.000000000000000000, 1.000000000000000000 ) ) ;
#4621=DIRECTION ( 'NONE',  ( 0.1305261922200524616, -0.9914448613738103822, 0.000000000000000000 ) ) ;
#4644=VERTEX_POINT ( 'NONE', #18232 ) ;
#4679=DIRECTION ( 'NONE',  ( 1.000000000000000000, 0.000000000000000000, 0.000000000000000000 ) ) ;
#4681=ORIENTED_EDGE ( 'NONE', *, *, #9594, .F. ) ;
#4695=DIRECTION ( 'NONE',  ( 0.000000000000000000, 0.000000000000000000, 1.000000000000000000 ) ) ;
#4718=EDGE_LOOP ( 'NONE', ( #3340, #2880, #7402, #8722 ) ) ;
#4725=( NAMED_UNIT ( * ) PLANE_ANGLE_UNIT ( ) SI_UNIT ( $, .RADIAN. ) );
#4735=ORIENTED_EDGE ( 'NONE', *, *, #8304, .F. ) ;
#4772=DIRECTION ( 'NONE',  ( 1.000000000000000000, 0.000000000000000000, 0.000000000000000000 ) ) ;
#4787=AXIS2_PLACEMENT_3D ( 'NONE', #3742, #903, #16792 ) ;
#4799=ORIENTED_EDGE ( 'NONE', *, *, #14024, .F. ) ;
#4828=CYLINDRICAL_SURFACE ( 'NONE', #9613, 0.7499999999999997780 ) ;
#4843=DIRECTION ( 'NONE',  ( 0.000000000000000000, 0.000000000000000000, 1.000000000000000000 ) ) ;
#4858=CIRCLE ( 'NONE', #6990, 4.799999999999999822 ) ;
#4861=ORIENTED_EDGE ( 'NONE', *, *, #2606, .F. ) ;
#4867=ORIENTED_EDGE ( 'NONE', *, *, #8308, .F. ) ;
#4875=ADVANCED_FACE ( 'NONE', ( #11705 ), #2668, .T. ) ;
#4896=CARTESIAN_POINT ( 'NONE',  ( -3.309651814758565180, -5.455921364805393026, 0.000000000000000000 ) ) ;
#4937=DIRECTION ( 'NONE',  ( 1.000000000000000000, 0.000000000000000000, 0.000000000000000000 ) ) ;
#4960=EDGE_LOOP ( 'NONE', ( #12556, #11023, #5095, #350 ) ) ;
#4961=EDGE_LOOP ( 'NONE', ( #16232, #17313, #4799, #7973 ) ) ;
#4981=VERTEX_POINT ( 'NONE', #5803 ) ;
#5000=VECTOR ( 'NONE', #16548, 1000.000000000000000 ) ;
#5007=LINE ( 'NONE', #299, #10840 ) ;
#5088=EDGE_CURVE ( 'NONE', #845, #16631, #4190, .T. ) ;
#5095=ORIENTED_EDGE ( 'NONE', *, *, #15882, .T. ) ;
#5115=DIRECTION ( 'NONE',  ( 0.000000000000000000, 0.000000000000000000, 1.000000000000000000 ) ) ;
#5124=DIRECTION ( 'NONE',  ( 1.000000000000000000, 0.000000000000000000, 0.000000000000000000 ) ) ;
#5209=EDGE_LOOP ( 'NONE', ( #9289, #4867 ) ) ;
#5235=CIRCLE ( 'NONE', #981, 0.7499999999999997780 ) ;
#5298=ADVANCED_FACE ( 'NONE', ( #15989 ), #14562, .T. ) ;
#5345=CIRCLE ( 'NONE', #8980, 0.7500000000000000000 ) ;
#5422=PLANE ( 'NONE',  #6161 ) ;
#5451=FACE_OUTER_BOUND ( 'NONE', #6798, .T. ) ;
#5454=ORIENTED_EDGE ( 'NONE', *, *, #10484, .F. ) ;
#5493=EDGE_LOOP ( 'NONE', ( #11221, #4105, #13045, #12475, #7588, #12766, #18255, #10439, #5993, #5677, #4587, #4546, #8896, #16981, #8446, #6815 ) ) ;
#5504=AXIS2_PLACEMENT_3D ( 'NONE', #4353, #8454, #11393 ) ;
#5522=CARTESIAN_POINT ( 'NONE',  ( -2.000000000000000000, -6.429618962271402616, 0.000000000000000000 ) ) ;
#5527=ORIENTED_EDGE ( 'NONE', *, *, #13557, .F. ) ;
#5574=AXIS2_PLACEMENT_3D ( 'NONE', #16824, #16734, #9568 ) ;
#5601=FACE_BOUND ( 'NONE', #6065, .T. ) ;
#5608=STYLED_ITEM ( 'NONE', ( #12339 ), #4227 ) ;
#5621=ADVANCED_FACE ( 'NONE', ( #9589 ), #15409, .T. ) ;
#5626=DIRECTION ( 'NONE',  ( 1.000000000000000000, 0.000000000000000000, 0.000000000000000000 ) ) ;
#5627=DIRECTION ( 'NONE',  ( 0.000000000000000000, 0.000000000000000000, 1.000000000000000000 ) ) ;
#5629=EDGE_CURVE ( 'NONE', #1871, #435, #7233, .T. ) ;
#5655=ORIENTED_EDGE ( 'NONE', *, *, #2483, .F. ) ;
#5677=ORIENTED_EDGE ( 'NONE', *, *, #14024, .T. ) ;
#5721=CARTESIAN_POINT ( 'NONE',  ( -4.078421086530219064, -3.990950201428956845, -1.000000000000000000 ) ) ;
#5752=CYLINDRICAL_SURFACE ( 'NONE', #8758, 2.396904916527700102 ) ;
#5755=CIRCLE ( 'NONE', #6662, 0.7500000000000000000 ) ;
#5759=VECTOR ( 'NONE', #8985, 1000.000000000000000 ) ;
#5788=DIRECTION ( 'NONE',  ( 0.000000000000000000, 0.000000000000000000, 1.000000000000000000 ) ) ;
#5803=CARTESIAN_POINT ( 'NONE',  ( 3.309651814758564736, -5.455921364805393026, 0.000000000000000000 ) ) ;
#5825=CARTESIAN_POINT ( 'NONE',  ( 0.1481481481481481122, -4.797713218419819903, -1.000000000000000000 ) ) ;
#5855=EDGE_CURVE ( 'NONE', #15649, #6911, #255, .T. ) ;
#5908=CARTESIAN_POINT ( 'NONE',  ( 5.686050877451574337, -5.768780236673276995, 0.000000000000000000 ) ) ;
#5909=DIRECTION ( 'NONE',  ( 0.000000000000000000, 0.000000000000000000, 1.000000000000000000 ) ) ;
#5960=DIRECTION ( 'NONE',  ( 1.000000000000000000, 0.000000000000000000, 0.000000000000000000 ) ) ;
#5993=ORIENTED_EDGE ( 'NONE', *, *, #2483, .T. ) ;
#6012=CARTESIAN_POINT ( 'NONE',  ( 4.078421086530217288, -3.990950201428958621, -1.000000000000000000 ) ) ;
#6049=CIRCLE ( 'NONE', #3812, 6.080745460913608902 ) ;
#6059=DIRECTION ( 'NONE',  ( 0.03086419753086420623, 0.9995235871707959241, -0.000000000000000000 ) ) ;
#6065=EDGE_LOOP ( 'NONE', ( #1973, #9461 ) ) ;
#6076=MECHANICAL_DESIGN_GEOMETRIC_PRESENTATION_REPRESENTATION('',(#17339),#17048);
#6137=VECTOR ( 'NONE', #2788, 1000.000000000000000 ) ;
#6143=DIRECTION ( 'NONE',  ( -0.9995235871707960351, -0.03086419753086420970, 0.000000000000000000 ) ) ;
#6161=AXIS2_PLACEMENT_3D ( 'NONE', #9596, #11402, #4083 ) ;
#6235=DIRECTION ( 'NONE',  ( 0.03086419753086420623, -0.9995235871707959241, 0.000000000000000000 ) ) ;
#6331=CARTESIAN_POINT ( 'NONE',  ( 4.799999999999999822, 0.000000000000000000, -1.000000000000000000 ) ) ;
#6358=CARTESIAN_POINT ( 'NONE',  ( 6.080745460913608902, 0.5192545390863916310, -1.000000000000000000 ) ) ;
#6390=FACE_OUTER_BOUND ( 'NONE', #17351, .T. ) ;
#6399=EDGE_CURVE ( 'NONE', #4564, #18729, #2399, .T. ) ;
#6402=ADVANCED_FACE ( 'NONE', ( #3567 ), #9360, .T. ) ;
#6413=ORIENTED_EDGE ( 'NONE', *, *, #6399, .T. ) ;
#6434=VERTEX_POINT ( 'NONE', #6606 ) ;
#6502=PLANE ( 'NONE',  #12637 ) ;
#6506=ADVANCED_FACE ( 'NONE', ( #14494 ), #11270, .F. ) ;
#6531=SURFACE_STYLE_USAGE ( .BOTH. , #16360 ) ;
#6551=CARTESIAN_POINT ( 'NONE',  ( 0.000000000000000000, 0.5192545390863916310, -1.000000000000000000 ) ) ;
#6560=CARTESIAN_POINT ( 'NONE',  ( -0.2500000000000000000, -8.096141056083446585, -1.000000000000000000 ) ) ;
#6592=DIRECTION ( 'NONE',  ( 0.000000000000000000, 0.000000000000000000, 1.000000000000000000 ) ) ;
#6606=CARTESIAN_POINT ( 'NONE',  ( -4.078421086530219064, -3.990950201428956845, 0.000000000000000000 ) ) ;
#6607=ORIENTED_EDGE ( 'NONE', *, *, #704, .F. ) ;
#6616=AXIS2_PLACEMENT_3D ( 'NONE', #17784, #4843, #10449 ) ;
#6620=ADVANCED_FACE ( 'NONE', ( #11915 ), #11833, .F. ) ;
#6662=AXIS2_PLACEMENT_3D ( 'NONE', #14100, #1166, #15631 ) ;
#6669=CIRCLE ( 'NONE', #10593, 6.080745460913608902 ) ;
#6680=EDGE_CURVE ( 'NONE', #14729, #12824, #6049, .T. ) ;
#6683=EDGE_CURVE ( 'NONE', #13795, #4644, #13255, .T. ) ;
#6775=ORIENTED_EDGE ( 'NONE', *, *, #7358, .F. ) ;
#6782=EDGE_CURVE ( 'NONE', #8150, #15649, #18220, .T. ) ;
#6798=EDGE_LOOP ( 'NONE', ( #4406, #10089, #8837, #6988 ) ) ;
#6815=ORIENTED_EDGE ( 'NONE', *, *, #5855, .T. ) ;
#6911=VERTEX_POINT ( 'NONE', #8298 ) ;
#6934=LINE ( 'NONE', #14164, #9647 ) ;
#6941=FACE_OUTER_BOUND ( 'NONE', #7812, .T. ) ;
#6949=CIRCLE ( 'NONE', #3300, 0.7499999999999997780 ) ;
#6966=AXIS2_PLACEMENT_3D ( 'NONE', #8363, #1038, #7980 ) ;
#6988=ORIENTED_EDGE ( 'NONE', *, *, #17068, .F. ) ;
#6990=AXIS2_PLACEMENT_3D ( 'NONE', #18345, #7013, #8536 ) ;
#7013=DIRECTION ( 'NONE',  ( -0.000000000000000000, -0.000000000000000000, -1.000000000000000000 ) ) ;
#7017=ORIENTED_EDGE ( 'NONE', *, *, #6680, .T. ) ;
#7040=VERTEX_POINT ( 'NONE', #2959 ) ;
#7058=DIRECTION ( 'NONE',  ( -1.000000000000000000, 0.000000000000000000, 0.000000000000000000 ) ) ;
#7069=LINE ( 'NONE', #17277, #16282 ) ;
#7106=ORIENTED_EDGE ( 'NONE', *, *, #16473, .T. ) ;
#7131=CARTESIAN_POINT ( 'NONE',  ( 4.799999999999999822, 0.000000000000000000, -1.000000000000000000 ) ) ;
#7170=DIRECTION ( 'NONE',  ( 0.000000000000000000, 0.000000000000000000, 1.000000000000000000 ) ) ;
#7188=CYLINDRICAL_SURFACE ( 'NONE', #14775, 2.396904916527699214 ) ;
#7192=AXIS2_PLACEMENT_3D ( 'NONE', #1043, #2179, #18565 ) ;
#7233=CIRCLE ( 'NONE', #18482, 0.7500000000000000000 ) ;
#7344=CARTESIAN_POINT ( 'NONE',  ( -3.309651814758565180, -5.455921364805393026, -1.000000000000000000 ) ) ;
#7358=EDGE_CURVE ( 'NONE', #14848, #806, #7597, .T. ) ;
#7388=ORIENTED_EDGE ( 'NONE', *, *, #14622, .F. ) ;
#7394=VERTEX_POINT ( 'NONE', #18624 ) ;
#7402=ORIENTED_EDGE ( 'NONE', *, *, #8304, .T. ) ;
#7434=VERTEX_POINT ( 'NONE', #4896 ) ;
#7440=ORIENTED_EDGE ( 'NONE', *, *, #4305, .F. ) ;
#7526=DIRECTION ( 'NONE',  ( 1.000000000000000000, 0.000000000000000000, 0.000000000000000000 ) ) ;
#7533=PLANE ( 'NONE',  #1774 ) ;
#7541=DIRECTION ( 'NONE',  ( 0.000000000000000000, 0.000000000000000000, 1.000000000000000000 ) ) ;
#7573=VERTEX_POINT ( 'NONE', #9751 ) ;
#7588=ORIENTED_EDGE ( 'NONE', *, *, #12858, .T. ) ;
#7594=ADVANCED_FACE ( 'NONE', ( #708, #12705, #2220 ), #18124, .T. ) ;
#7597=CIRCLE ( 'NONE', #16434, 4.799999999999999822 ) ;
#7618=AXIS2_PLACEMENT_3D ( 'NONE', #9162, #12298, #7728 ) ;
#7621=CARTESIAN_POINT ( 'NONE',  ( -0.5000000000000000000, -6.429618962271402616, -1.000000000000000000 ) ) ;
#7649=DIRECTION ( 'NONE',  ( 0.000000000000000000, 0.000000000000000000, 1.000000000000000000 ) ) ;
#7676=AXIS2_PLACEMENT_3D ( 'NONE', #2089, #1887, #4937 ) ;
#7728=DIRECTION ( 'NONE',  ( 1.000000000000000000, 0.000000000000000000, 0.000000000000000000 ) ) ;
#7757=ORIENTED_EDGE ( 'NONE', *, *, #5088, .F. ) ;
#7766=( NAMED_UNIT ( * ) SI_UNIT ( $, .STERADIAN. ) SOLID_ANGLE_UNIT ( ) );
#7782=ADVANCED_FACE ( 'NONE', ( #15845 ), #5752, .F. ) ;
#7812=EDGE_LOOP ( 'NONE', ( #16998, #4735, #3648, #11585, #14496, #5454, #3027, #8585, #1210, #12326, #4681, #2061, #161, #722, #5527, #6775 ) ) ;
#7861=CARTESIAN_POINT ( 'NONE',  ( 0.000000000000000000, 0.000000000000000000, -1.000000000000000000 ) ) ;
#7878=VECTOR ( 'NONE', #17642, 1000.000000000000000 ) ;
#7942=EDGE_CURVE ( 'NONE', #9997, #8150, #6949, .T. ) ;
#7972=DIRECTION ( 'NONE',  ( 0.000000000000000000, 0.000000000000000000, 1.000000000000000000 ) ) ;
#7973=ORIENTED_EDGE ( 'NONE', *, *, #10936, .F. ) ;
#7980=DIRECTION ( 'NONE',  ( 1.000000000000000000, 0.000000000000000000, 0.000000000000000000 ) ) ;
#8012=VERTEX_POINT ( 'NONE', #974 ) ;
#8017=AXIS2_PLACEMENT_3D ( 'NONE', #12801, #14324, #9934 ) ;
#8040=DIRECTION ( 'NONE',  ( -0.000000000000000000, -0.000000000000000000, -1.000000000000000000 ) ) ;
#8092=AXIS2_PLACEMENT_3D ( 'NONE', #2589, #8404, #16883 ) ;
#8150=VERTEX_POINT ( 'NONE', #16780 ) ;
#8175=CARTESIAN_POINT ( 'NONE',  ( -0.2500000000000000000, -8.096141056083446585, -1.000000000000000000 ) ) ;
#8194=EDGE_CURVE ( 'NONE', #2784, #14848, #17586, .T. ) ;
#8239=CARTESIAN_POINT ( 'NONE',  ( 0.5000000000000000000, -6.429618962271402616, -1.000000000000000000 ) ) ;
#8241=AXIS2_PLACEMENT_3D ( 'NONE', #12210, #6592, #18018 ) ;
#8265=CARTESIAN_POINT ( 'NONE',  ( -4.799999999999999822, 5.878304635907294211E-16, -1.000000000000000000 ) ) ;
#8285=EDGE_LOOP ( 'NONE', ( #2116, #15378, #1335, #9368 ) ) ;
#8291=ADVANCED_FACE ( 'NONE', ( #5451 ), #11434, .F. ) ;
#8294=CARTESIAN_POINT ( 'NONE',  ( -3.309651814758565180, -5.455921364805393026, -1.000000000000000000 ) ) ;
#8298=CARTESIAN_POINT ( 'NONE',  ( -0.1481481481481481122, -4.797713218419819903, 0.000000000000000000 ) ) ;
#8300=PRODUCT_DEFINITION ( 'UNKNOWN', '', #10485, #1225 ) ;
#8304=EDGE_CURVE ( 'NONE', #276, #2784, #2573, .T. ) ;
#8308=EDGE_CURVE ( 'NONE', #168, #8012, #5755, .T. ) ;
#8320=DIRECTION ( 'NONE',  ( 0.000000000000000000, 0.000000000000000000, 1.000000000000000000 ) ) ;
#8332=CARTESIAN_POINT ( 'NONE',  ( 5.686050877451574337, -5.768780236673276995, -1.000000000000000000 ) ) ;
#8360=ORIENTED_EDGE ( 'NONE', *, *, #6683, .T. ) ;
#8363=CARTESIAN_POINT ( 'NONE',  ( -1.250000000000000000, -6.429618962271402616, -1.000000000000000000 ) ) ;
#8394=CARTESIAN_POINT ( 'NONE',  ( 2.354826896168714434, -6.962563485461402024, 0.000000000000000000 ) ) ;
#8404=DIRECTION ( 'NONE',  ( -0.000000000000000000, -0.000000000000000000, -1.000000000000000000 ) ) ;
#8446=ORIENTED_EDGE ( 'NONE', *, *, #6782, .T. ) ;
#8454=DIRECTION ( 'NONE',  ( 0.000000000000000000, 0.000000000000000000, 1.000000000000000000 ) ) ;
#8463=CARTESIAN_POINT ( 'NONE',  ( -0.1481481481481481122, -4.797713218419819903, -1.000000000000000000 ) ) ;
#8536=DIRECTION ( 'NONE',  ( 1.000000000000000000, 0.000000000000000000, 0.000000000000000000 ) ) ;
#8547=LINE ( 'NONE', #12931, #17490 ) ;
#8554=ORIENTED_EDGE ( 'NONE', *, *, #935, .T. ) ;
#8568=DIRECTION ( 'NONE',  ( 0.000000000000000000, 0.000000000000000000, 1.000000000000000000 ) ) ;
#8585=ORIENTED_EDGE ( 'NONE', *, *, #17782, .F. ) ;
#8628=CARTESIAN_POINT ( 'NONE',  ( -2.595115354961444076, -7.673029147243174641, -1.000000000000000000 ) ) ;
#8717=AXIS2_PLACEMENT_3D ( 'NONE', #1424, #8568, #17343 ) ;
#8722=ORIENTED_EDGE ( 'NONE', *, *, #17068, .T. ) ;
#8758=AXIS2_PLACEMENT_3D ( 'NONE', #1281, #1464, #14599 ) ;
#8778=LINE ( 'NONE', #13163, #1417 ) ;
#8827=DIRECTION ( 'NONE',  ( 0.9995235871707960351, -0.03086419753086420970, 0.000000000000000000 ) ) ;
#8837=ORIENTED_EDGE ( 'NONE', *, *, #18275, .F. ) ;
#8858=DIRECTION ( 'NONE',  ( 1.000000000000000000, 0.000000000000000000, 0.000000000000000000 ) ) ;
#8883=LINE ( 'NONE', #13272, #11261 ) ;
#8891=AXIS2_PLACEMENT_3D ( 'NONE', #4277, #8827, #14442 ) ;
#8896=ORIENTED_EDGE ( 'NONE', *, *, #13816, .T. ) ;
#8905=CARTESIAN_POINT ( 'NONE',  ( 0.1481481481481481122, -4.797713218419819903, -1.000000000000000000 ) ) ;
#8941=( GEOMETRIC_REPRESENTATION_CONTEXT ( 3 ) GLOBAL_UNCERTAINTY_ASSIGNED_CONTEXT ( ( #2743 ) ) GLOBAL_UNIT_ASSIGNED_CONTEXT ( ( #3690, #4725, #12060 ) ) REPRESENTATION_CONTEXT ( 'NONE', 'WORKASPACE' ) );
#8962=AXIS2_PLACEMENT_3D ( 'NONE', #1763, #1580, #430 ) ;
#8980=AXIS2_PLACEMENT_3D ( 'NONE', #3157, #10474, #391 ) ;
#8985=DIRECTION ( 'NONE',  ( 0.000000000000000000, 0.000000000000000000, 1.000000000000000000 ) ) ;
#9002=VERTEX_POINT ( 'NONE', #6358 ) ;
#9004=CARTESIAN_POINT ( 'NONE',  ( 2.354826896168714434, -6.962563485461402024, -1.000000000000000000 ) ) ;
#9011=VECTOR ( 'NONE', #3369, 1000.000000000000000 ) ;
#9102=EDGE_CURVE ( 'NONE', #2539, #16873, #4858, .T. ) ;
#9131=CARTESIAN_POINT ( 'NONE',  ( 4.799999999999999822, 0.000000000000000000, 0.000000000000000000 ) ) ;
#9151=DIRECTION ( 'NONE',  ( 0.000000000000000000, 0.000000000000000000, 1.000000000000000000 ) ) ;
#9162=CARTESIAN_POINT ( 'NONE',  ( 0.000000000000000000, 0.5192545390863916310, -1.000000000000000000 ) ) ;
#9242=MANIFOLD_SOLID_BREP ( 'Body', #17433 ) ;
#9264=FACE_OUTER_BOUND ( 'NONE', #13459, .T. ) ;
#9289=ORIENTED_EDGE ( 'NONE', *, *, #12500, .F. ) ;
#9307=CIRCLE ( 'NONE', #8092, 2.396904916527700102 ) ;
#9309=CARTESIAN_POINT ( 'NONE',  ( 3.098410542199072637, -7.060458129626440815, 0.000000000000000000 ) ) ;
#9322=ORIENTED_EDGE ( 'NONE', *, *, #686, .F. ) ;
#9351=CIRCLE ( 'NONE', #4787, 0.7500000000000000000 ) ;
#9360=CYLINDRICAL_SURFACE ( 'NONE', #11204, 6.080745460913608902 ) ;
#9366=VECTOR ( 'NONE', #6059, 1000.000000000000114 ) ;
#9368=ORIENTED_EDGE ( 'NONE', *, *, #2154, .T. ) ;
#9372=AXIS2_PLACEMENT_3D ( 'NONE', #11342, #1261, #5626 ) ;
#9397=FILL_AREA_STYLE_COLOUR ( '', #18065 ) ;
#9450=( NAMED_UNIT ( * ) SI_UNIT ( $, .STERADIAN. ) SOLID_ANGLE_UNIT ( ) );
#9458=CARTESIAN_POINT ( 'NONE',  ( 0.1481481481481481122, -4.797713218419819903, -1.000000000000000000 ) ) ;
#9461=ORIENTED_EDGE ( 'NONE', *, *, #5088, .T. ) ;
#9526=CARTESIAN_POINT ( 'NONE',  ( 0.000000000000000000, 0.000000000000000000, 0.000000000000000000 ) ) ;
#9530=AXIS2_PLACEMENT_3D ( 'NONE', #11852, #7649, #3570 ) ;
#9568=DIRECTION ( 'NONE',  ( 1.000000000000000000, 0.000000000000000000, 0.000000000000000000 ) ) ;
#9589=FACE_OUTER_BOUND ( 'NONE', #10562, .T. ) ;
#9594=EDGE_CURVE ( 'NONE', #7040, #12093, #13179, .T. ) ;
#9596=CARTESIAN_POINT ( 'NONE',  ( 0.000000000000000000, 0.000000000000000000, -1.000000000000000000 ) ) ;
#9610=AXIS2_PLACEMENT_3D ( 'NONE', #1288, #7170, #14240 ) ;
#9613=AXIS2_PLACEMENT_3D ( 'NONE', #9004, #351, #5960 ) ;
#9620=DIRECTION ( 'NONE',  ( 1.000000000000000000, 0.000000000000000000, 0.000000000000000000 ) ) ;
#9644=AXIS2_PLACEMENT_3D ( 'NONE', #13159, #7972, #14868 ) ;
#9647=VECTOR ( 'NONE', #4604, 1000.000000000000000 ) ;
#9710=EDGE_CURVE ( 'NONE', #13795, #9002, #15224, .T. ) ;
#9716=ORIENTED_EDGE ( 'NONE', *, *, #8308, .T. ) ;
#9748=CARTESIAN_POINT ( 'NONE',  ( -1.250000000000000000, -6.429618962271402616, -1.000000000000000000 ) ) ;
#9751=CARTESIAN_POINT ( 'NONE',  ( 2.595115354961440524, -7.673029147243177306, -1.000000000000000000 ) ) ;
#9763=EDGE_CURVE ( 'NONE', #15974, #6434, #16134, .T. ) ;
#9788=DIRECTION ( 'NONE',  ( 0.000000000000000000, 0.000000000000000000, 1.000000000000000000 ) ) ;
#9814=CARTESIAN_POINT ( 'NONE',  ( 0.000000000000000000, 0.000000000000000000, 0.000000000000000000 ) ) ;
#9864=APPLICATION_CONTEXT ( 'automotive_design' ) ;
#9918=ADVANCED_FACE ( 'NONE', ( #4488 ), #14762, .T. ) ;
#9929=DIRECTION ( 'NONE',  ( 0.000000000000000000, 0.000000000000000000, 1.000000000000000000 ) ) ;
#9934=DIRECTION ( 'NONE',  ( 1.000000000000000000, 0.000000000000000000, 0.000000000000000000 ) ) ;
#9971=DIRECTION ( 'NONE',  ( 0.000000000000000000, 0.000000000000000000, 1.000000000000000000 ) ) ;
#9977=ORIENTED_EDGE ( 'NONE', *, *, #10210, .T. ) ;
#9997=VERTEX_POINT ( 'NONE', #116 ) ;
#10008=CIRCLE ( 'NONE', #6966, 0.7500000000000000000 ) ;
#10015=AXIS2_PLACEMENT_3D ( 'NONE', #9526, #17920, #10674 ) ;
#10052=CARTESIAN_POINT ( 'NONE',  ( 0.000000000000000000, 0.000000000000000000, -1.000000000000000000 ) ) ;
#10079=EDGE_CURVE ( 'NONE', #1489, #1871, #14869, .T. ) ;
#10089=ORIENTED_EDGE ( 'NONE', *, *, #12971, .T. ) ;
#10109=EDGE_CURVE ( 'NONE', #18729, #8150, #15595, .T. ) ;
#10123=EDGE_LOOP ( 'NONE', ( #10263, #7017, #1754, #1850 ) ) ;
#10127=ORIENTED_EDGE ( 'NONE', *, *, #12971, .F. ) ;
#10196=CARTESIAN_POINT ( 'NONE',  ( -3.098410542199071749, -7.060458129626440815, -1.000000000000000000 ) ) ;
#10210=EDGE_CURVE ( 'NONE', #7394, #7573, #3070, .T. ) ;
#10243=AXIS2_PLACEMENT_3D ( 'NONE', #14005, #17152, #18375 ) ;
#10244=CIRCLE ( 'NONE', #8717, 8.099999999999999645 ) ;
#10252=DIRECTION ( 'NONE',  ( 1.000000000000000000, 0.000000000000000000, 0.000000000000000000 ) ) ;
#10263=ORIENTED_EDGE ( 'NONE', *, *, #14704, .F. ) ;
#10306=DIRECTION ( 'NONE',  ( 0.1305261922200524616, -0.9914448613738103822, 0.000000000000000000 ) ) ;
#10373=LINE ( 'NONE', #15997, #2318 ) ;
#10431=EDGE_LOOP ( 'NONE', ( #7757, #4278, #9716, #11586 ) ) ;
#10439=ORIENTED_EDGE ( 'NONE', *, *, #14622, .T. ) ;
#10449=DIRECTION ( 'NONE',  ( 1.000000000000000000, 0.000000000000000000, 0.000000000000000000 ) ) ;
#10466=CYLINDRICAL_SURFACE ( 'NONE', #9644, 8.099999999999999645 ) ;
#10474=DIRECTION ( 'NONE',  ( 0.000000000000000000, 0.000000000000000000, 1.000000000000000000 ) ) ;
#10484=EDGE_CURVE ( 'NONE', #12824, #17009, #1267, .T. ) ;
#10485=PRODUCT_DEFINITION_FORMATION_WITH_SPECIFIED_SOURCE ( 'ANY', '', #2666, .NOT_KNOWN. ) ;
#10495=DIRECTION ( 'NONE',  ( 0.000000000000000000, 0.000000000000000000, 1.000000000000000000 ) ) ;
#10562=EDGE_LOOP ( 'NONE', ( #16584, #12082, #9977, #14320 ) ) ;
#10586=EDGE_LOOP ( 'NONE', ( #4861, #13303, #14639, #4090 ) ) ;
#10588=ORIENTED_EDGE ( 'NONE', *, *, #10793, .F. ) ;
#10593=AXIS2_PLACEMENT_3D ( 'NONE', #17986, #1979, #13616 ) ;
#10674=DIRECTION ( 'NONE',  ( 1.000000000000000000, 0.000000000000000000, 0.000000000000000000 ) ) ;
#10716=EDGE_LOOP ( 'NONE', ( #13462, #13690 ) ) ;
#10723=CIRCLE ( 'NONE', #12883, 0.7499999999999997780 ) ;
#10782=DIRECTION ( 'NONE',  ( 1.000000000000000000, 0.000000000000000000, -0.000000000000000000 ) ) ;
#10793=EDGE_CURVE ( 'NONE', #15209, #435, #8883, .T. ) ;
#10817=DIRECTION ( 'NONE',  ( 0.000000000000000000, 0.000000000000000000, 1.000000000000000000 ) ) ;
#10840=VECTOR ( 'NONE', #5115, 1000.000000000000000 ) ;
#10849=DIRECTION ( 'NONE',  ( -0.9914448613738102711, -0.1305261922200524338, 0.000000000000000000 ) ) ;
#10911=ORIENTED_EDGE ( 'NONE', *, *, #10936, .T. ) ;
#10923=ORIENTED_EDGE ( 'NONE', *, *, #3716, .F. ) ;
#10936=EDGE_CURVE ( 'NONE', #9002, #1826, #12499, .T. ) ;
#10962=VECTOR ( 'NONE', #11010, 1000.000000000000000 ) ;
#11010=DIRECTION ( 'NONE',  ( 0.000000000000000000, 0.000000000000000000, 1.000000000000000000 ) ) ;
#11023=ORIENTED_EDGE ( 'NONE', *, *, #13557, .T. ) ;
#11100=EDGE_CURVE ( 'NONE', #6434, #7434, #9307, .T. ) ;
#11138=LINE ( 'NONE', #8294, #14254 ) ;
#11151=CIRCLE ( 'NONE', #14813, 2.396904916527699214 ) ;
#11204=AXIS2_PLACEMENT_3D ( 'NONE', #15188, #16710, #13748 ) ;
#11221=ORIENTED_EDGE ( 'NONE', *, *, #18275, .T. ) ;
#11236=ORIENTED_EDGE ( 'NONE', *, *, #9594, .T. ) ;
#11251=DIRECTION ( 'NONE',  ( 0.000000000000000000, 0.000000000000000000, 1.000000000000000000 ) ) ;
#11261=VECTOR ( 'NONE', #10495, 1000.000000000000000 ) ;
#11270=CYLINDRICAL_SURFACE ( 'NONE', #16085, 0.7500000000000000000 ) ;
#11272=EDGE_CURVE ( 'NONE', #17009, #4564, #8778, .T. ) ;
#11305=UNCERTAINTY_MEASURE_WITH_UNIT (LENGTH_MEASURE( 1.000000000000000082E-05 ), #18056, 'distance_accuracy_value', 'NONE');
#11342=CARTESIAN_POINT ( 'NONE',  ( 0.000000000000000000, 0.000000000000000000, -1.000000000000000000 ) ) ;
#11365=ORIENTED_EDGE ( 'NONE', *, *, #2154, .F. ) ;
#11393=DIRECTION ( 'NONE',  ( 1.000000000000000000, 0.000000000000000000, 0.000000000000000000 ) ) ;
#11402=DIRECTION ( 'NONE',  ( 0.000000000000000000, 0.000000000000000000, 1.000000000000000000 ) ) ;
#11434=CYLINDRICAL_SURFACE ( 'NONE', #1480, 4.799999999999999822 ) ;
#11498=AXIS2_PLACEMENT_3D ( 'NONE', #2358, #9788, #10252 ) ;
#11502=AXIS2_PLACEMENT_3D ( 'NONE', #13944, #15359, #10782 ) ;
#11525=EDGE_CURVE ( 'NONE', #2085, #2539, #15732, .T. ) ;
#11585=ORIENTED_EDGE ( 'NONE', *, *, #6399, .F. ) ;
#11586=ORIENTED_EDGE ( 'NONE', *, *, #12321, .F. ) ;
#11668=DIRECTION ( 'NONE',  ( -0.000000000000000000, -0.000000000000000000, -1.000000000000000000 ) ) ;
#11677=DIRECTION ( 'NONE',  ( 1.000000000000000000, 0.000000000000000000, 0.000000000000000000 ) ) ;
#11705=FACE_OUTER_BOUND ( 'NONE', #15514, .T. ) ;
#11766=ORIENTED_EDGE ( 'NONE', *, *, #1665, .F. ) ;
#11775=ORIENTED_EDGE ( 'NONE', *, *, #11525, .F. ) ;
#11785=ORIENTED_EDGE ( 'NONE', *, *, #1205, .T. ) ;
#11833=CYLINDRICAL_SURFACE ( 'NONE', #17606, 0.7500000000000000000 ) ;
#11848=CARTESIAN_POINT ( 'NONE',  ( 3.309651814758564736, -5.455921364805393026, -1.000000000000000000 ) ) ;
#11852=CARTESIAN_POINT ( 'NONE',  ( 0.000000000000000000, 0.000000000000000000, -1.000000000000000000 ) ) ;
#11915=FACE_OUTER_BOUND ( 'NONE', #17497, .T. ) ;
#12060=( NAMED_UNIT ( * ) SI_UNIT ( $, .STERADIAN. ) SOLID_ANGLE_UNIT ( ) );
#12082=ORIENTED_EDGE ( 'NONE', *, *, #1352, .F. ) ;
#12093=VERTEX_POINT ( 'NONE', #11848 ) ;
#12136=EDGE_CURVE ( 'NONE', #7040, #17682, #8547, .T. ) ;
#12164=SHAPE_REPRESENTATION_RELATIONSHIP ( 'NONE' , 'NONE' ,  #434, #4227 ) ;
#12210=CARTESIAN_POINT ( 'NONE',  ( 0.000000000000000000, 0.5192545390863916310, 0.000000000000000000 ) ) ;
#12232=DIRECTION ( 'NONE',  ( 0.000000000000000000, 0.000000000000000000, 1.000000000000000000 ) ) ;
#12258=ADVANCED_FACE ( 'NONE', ( #700 ), #6502, .T. ) ;
#12298=DIRECTION ( 'NONE',  ( 0.000000000000000000, 0.000000000000000000, 1.000000000000000000 ) ) ;
#12304=CARTESIAN_POINT ( 'NONE',  ( 3.309651814758565180, -5.455921364805393026, -1.000000000000000000 ) ) ;
#12315=ORIENTED_EDGE ( 'NONE', *, *, #6683, .F. ) ;
#12321=EDGE_CURVE ( 'NONE', #16631, #8012, #7069, .T. ) ;
#12326=ORIENTED_EDGE ( 'NONE', *, *, #935, .F. ) ;
#12339=PRESENTATION_STYLE_ASSIGNMENT (( #6531 ) ) ;
#12358=DIRECTION ( 'NONE',  ( 0.000000000000000000, 0.000000000000000000, 1.000000000000000000 ) ) ;
#12413=DIRECTION ( 'NONE',  ( 0.03086419753086420623, -0.9995235871707959241, 0.000000000000000000 ) ) ;
#12423=VECTOR ( 'NONE', #14400, 1000.000000000000000 ) ;
#12429=AXIS2_PLACEMENT_3D ( 'NONE', #13941, #16600, #907 ) ;
#12475=ORIENTED_EDGE ( 'NONE', *, *, #15442, .T. ) ;
#12488=EDGE_LOOP ( 'NONE', ( #10588, #11766, #13682, #18384 ) ) ;
#12493=EDGE_CURVE ( 'NONE', #435, #1871, #5345, .T. ) ;
#12499=LINE ( 'NONE', #16417, #9011 ) ;
#12500=EDGE_CURVE ( 'NONE', #8012, #168, #18726, .T. ) ;
#12516=AXIS2_PLACEMENT_3D ( 'NONE', #17957, #8040, #13683 ) ;
#12554=FACE_BOUND ( 'NONE', #10716, .T. ) ;
#12556=ORIENTED_EDGE ( 'NONE', *, *, #2346, .F. ) ;
#12637=AXIS2_PLACEMENT_3D ( 'NONE', #12304, #16708, #3658 ) ;
#12672=DIRECTION ( 'NONE',  ( -1.000000000000000000, 0.000000000000000000, 0.000000000000000000 ) ) ;
#12698=AXIS2_PLACEMENT_3D ( 'NONE', #7861, #12232, #17761 ) ;
#12705=FACE_BOUND ( 'NONE', #5209, .T. ) ;
#12766=ORIENTED_EDGE ( 'NONE', *, *, #3, .T. ) ;
#12801=CARTESIAN_POINT ( 'NONE',  ( 0.000000000000000000, 0.000000000000000000, 0.000000000000000000 ) ) ;
#12824=VERTEX_POINT ( 'NONE', #5721 ) ;
#12840=CARTESIAN_POINT ( 'NONE',  ( 2.000000000000000000, -6.429618962271402616, -1.000000000000000000 ) ) ;
#12858=EDGE_CURVE ( 'NONE', #3875, #2619, #2935, .T. ) ;
#12882=CIRCLE ( 'NONE', #5574, 4.799999999999999822 ) ;
#12883=AXIS2_PLACEMENT_3D ( 'NONE', #8394, #5627, #7058 ) ;
#12901=SHAPE_DEFINITION_REPRESENTATION ( #18632, #434 ) ;
#12916=CARTESIAN_POINT ( 'NONE',  ( 5.686050877451574337, -5.768780236673276995, -1.000000000000000000 ) ) ;
#12931=CARTESIAN_POINT ( 'NONE',  ( 3.098410542199072637, -7.060458129626440815, -1.000000000000000000 ) ) ;
#12942=AXIS2_PLACEMENT_3D ( 'NONE', #8905, #6143, #6235 ) ;
#12971=EDGE_CURVE ( 'NONE', #14848, #2085, #10373, .T. ) ;
#13011=EDGE_LOOP ( 'NONE', ( #14732, #609, #11236, #16449 ) ) ;
#13045=ORIENTED_EDGE ( 'NONE', *, *, #9102, .T. ) ;
#13159=CARTESIAN_POINT ( 'NONE',  ( 0.000000000000000000, 0.000000000000000000, -1.000000000000000000 ) ) ;
#13163=CARTESIAN_POINT ( 'NONE',  ( -3.309651814758565180, -5.455921364805393026, -1.000000000000000000 ) ) ;
#13179=LINE ( 'NONE', #1474, #18262 ) ;
#13198=ADVANCED_FACE ( 'NONE', ( #3020 ), #4535, .F. ) ;
#13199=ADVANCED_FACE ( 'NONE', ( #3199 ), #69, .T. ) ;
#13207=DIRECTION ( 'NONE',  ( 1.000000000000000000, 0.000000000000000000, 0.000000000000000000 ) ) ;
#13239=CARTESIAN_POINT ( 'NONE',  ( 0.5000000000000000000, -6.429618962271402616, 0.000000000000000000 ) ) ;
#13252=CARTESIAN_POINT ( 'NONE',  ( 0.1481481481481481122, -4.797713218419819903, -1.000000000000000000 ) ) ;
#13255=LINE ( 'NONE', #6012, #7878 ) ;
#13272=CARTESIAN_POINT ( 'NONE',  ( -2.000000000000000000, -6.429618962271402616, -1.000000000000000000 ) ) ;
#13303=ORIENTED_EDGE ( 'NONE', *, *, #10793, .T. ) ;
#13351=FACE_OUTER_BOUND ( 'NONE', #346, .T. ) ;
#13398=CARTESIAN_POINT ( 'NONE',  ( -2.000000000000000000, -6.429618962271402616, -1.000000000000000000 ) ) ;
#13459=EDGE_LOOP ( 'NONE', ( #10127, #930, #853, #11775 ) ) ;
#13462=ORIENTED_EDGE ( 'NONE', *, *, #1665, .T. ) ;
#13473=ORIENTED_EDGE ( 'NONE', *, *, #11272, .T. ) ;
#13557=EDGE_CURVE ( 'NONE', #806, #17177, #1685, .T. ) ;
#13583=CYLINDRICAL_SURFACE ( 'NONE', #12698, 4.799999999999999822 ) ;
#13600=VECTOR ( 'NONE', #3553, 999.9999999999998863 ) ;
#13611=LINE ( 'NONE', #8175, #5000 ) ;
#13616=DIRECTION ( 'NONE',  ( 1.000000000000000000, 0.000000000000000000, 0.000000000000000000 ) ) ;
#13617=FACE_OUTER_BOUND ( 'NONE', #10586, .T. ) ;
#13682=ORIENTED_EDGE ( 'NONE', *, *, #10079, .T. ) ;
#13683=DIRECTION ( 'NONE',  ( 1.000000000000000000, 0.000000000000000000, 0.000000000000000000 ) ) ;
#13690=ORIENTED_EDGE ( 'NONE', *, *, #2606, .T. ) ;
#13748=DIRECTION ( 'NONE',  ( 1.000000000000000000, 0.000000000000000000, 0.000000000000000000 ) ) ;
#13757=DIRECTION ( 'NONE',  ( 0.000000000000000000, 0.000000000000000000, 1.000000000000000000 ) ) ;
#13795=VERTEX_POINT ( 'NONE', #1762 ) ;
#13816=EDGE_CURVE ( 'NONE', #7434, #9997, #3387, .T. ) ;
#13941=CARTESIAN_POINT ( 'NONE',  ( -2.354826896168714434, -6.962563485461402024, -1.000000000000000000 ) ) ;
#13944=CARTESIAN_POINT ( 'NONE',  ( 0.000000000000000000, 0.000000000000000000, 0.000000000000000000 ) ) ;
#14005=CARTESIAN_POINT ( 'NONE',  ( 0.000000000000000000, 0.000000000000000000, 0.000000000000000000 ) ) ;
#14023=AXIS2_PLACEMENT_3D ( 'NONE', #3064, #5909, #8858 ) ;
#14024=EDGE_CURVE ( 'NONE', #1826, #15974, #807, .T. ) ;
#14100=CARTESIAN_POINT ( 'NONE',  ( 1.250000000000000000, -6.429618962271402616, 0.000000000000000000 ) ) ;
#14102=VECTOR ( 'NONE', #12413, 1000.000000000000114 ) ;
#14127=DIRECTION ( 'NONE',  ( -0.000000000000000000, -0.000000000000000000, -1.000000000000000000 ) ) ;
#14164=CARTESIAN_POINT ( 'NONE',  ( 0.2499999999999966416, -8.096141056083448362, -1.000000000000000000 ) ) ;
#14240=DIRECTION ( 'NONE',  ( 1.000000000000000000, 0.000000000000000000, 0.000000000000000000 ) ) ;
#14254=VECTOR ( 'NONE', #881, 1000.000000000000000 ) ;
#14320=ORIENTED_EDGE ( 'NONE', *, *, #704, .T. ) ;
#14324=DIRECTION ( 'NONE',  ( 0.000000000000000000, 0.000000000000000000, 1.000000000000000000 ) ) ;
#14342=DIRECTION ( 'NONE',  ( 0.000000000000000000, 0.000000000000000000, 1.000000000000000000 ) ) ;
#14376=CARTESIAN_POINT ( 'NONE',  ( 0.000000000000000000, 0.5192545390863916310, -1.000000000000000000 ) ) ;
#14388=EDGE_CURVE ( 'NONE', #17682, #4981, #15455, .T. ) ;
#14400=DIRECTION ( 'NONE',  ( 0.000000000000000000, 0.000000000000000000, 1.000000000000000000 ) ) ;
#14426=EDGE_LOOP ( 'NONE', ( #17101, #7440, #6413, #317 ) ) ;
#14428=LINE ( 'NONE', #10196, #18117 ) ;
#14442=DIRECTION ( 'NONE',  ( 0.03086419753086420623, 0.9995235871707959241, 0.000000000000000000 ) ) ;
#14494=FACE_OUTER_BOUND ( 'NONE', #12488, .T. ) ;
#14496=ORIENTED_EDGE ( 'NONE', *, *, #11272, .F. ) ;
#14519=AXIS2_PLACEMENT_3D ( 'NONE', #3417, #3225, #18070 ) ;
#14522=DIRECTION ( 'NONE',  ( 1.000000000000000000, 0.000000000000000000, 0.000000000000000000 ) ) ;
#14562=CYLINDRICAL_SURFACE ( 'NONE', #14519, 6.080745460913608902 ) ;
#14575=ORIENTED_EDGE ( 'NONE', *, *, #12321, .T. ) ;
#14599=DIRECTION ( 'NONE',  ( 1.000000000000000000, 0.000000000000000000, 0.000000000000000000 ) ) ;
#14600=ORIENTED_EDGE ( 'NONE', *, *, #6782, .F. ) ;
#14606=ORIENTED_EDGE ( 'NONE', *, *, #12493, .F. ) ;
#14611=EDGE_CURVE ( 'NONE', #845, #168, #5007, .T. ) ;
#14622=EDGE_CURVE ( 'NONE', #4981, #4644, #840, .T. ) ;
#14639=ORIENTED_EDGE ( 'NONE', *, *, #12493, .T. ) ;
#14704=EDGE_CURVE ( 'NONE', #14729, #15974, #3063, .T. ) ;
#14713=ADVANCED_FACE ( 'NONE', ( #13351 ), #10466, .T. ) ;
#14726=APPLICATION_CONTEXT ( 'automotive_design' ) ;
#14729=VERTEX_POINT ( 'NONE', #1815 ) ;
#14732=ORIENTED_EDGE ( 'NONE', *, *, #14388, .F. ) ;
#14762=CYLINDRICAL_SURFACE ( 'NONE', #14023, 0.7499999999999997780 ) ;
#14775=AXIS2_PLACEMENT_3D ( 'NONE', #12916, #14342, #14522 ) ;
#14807=LINE ( 'NONE', #2321, #16646 ) ;
#14813=AXIS2_PLACEMENT_3D ( 'NONE', #8332, #14127, #17100 ) ;
#14848=VERTEX_POINT ( 'NONE', #8265 ) ;
#14868=DIRECTION ( 'NONE',  ( 1.000000000000000000, 0.000000000000000000, 0.000000000000000000 ) ) ;
#14869=LINE ( 'NONE', #7621, #10962 ) ;
#14876=DIRECTION ( 'NONE',  ( 0.1305261922200524338, -0.9914448613738102711, 0.000000000000000000 ) ) ;
#14921=CARTESIAN_POINT ( 'NONE',  ( -0.1481481481481481122, -4.797713218419819903, 0.000000000000000000 ) ) ;
#15011=FACE_OUTER_BOUND ( 'NONE', #4960, .T. ) ;
#15022=SURFACE_STYLE_FILL_AREA ( #444 ) ;
#15048=ORIENTED_EDGE ( 'NONE', *, *, #13816, .F. ) ;
#15073=ADVANCED_FACE ( 'NONE', ( #15011 ), #13583, .F. ) ;
#15181=( NAMED_UNIT ( * ) PLANE_ANGLE_UNIT ( ) SI_UNIT ( $, .RADIAN. ) );
#15188=CARTESIAN_POINT ( 'NONE',  ( 0.000000000000000000, 0.5192545390863916310, -1.000000000000000000 ) ) ;
#15209=VERTEX_POINT ( 'NONE', #13398 ) ;
#15222=CARTESIAN_POINT ( 'NONE',  ( -6.080745460913608902, 0.5192545390863924082, -1.000000000000000000 ) ) ;
#15224=CIRCLE ( 'NONE', #7618, 6.080745460913608902 ) ;
#15254=ORIENTED_EDGE ( 'NONE', *, *, #18740, .T. ) ;
#15286=CIRCLE ( 'NONE', #2513, 6.080745460913608902 ) ;
#15359=DIRECTION ( 'NONE',  ( 0.000000000000000000, 0.000000000000000000, 1.000000000000000000 ) ) ;
#15378=ORIENTED_EDGE ( 'NONE', *, *, #3307, .F. ) ;
#15409=CYLINDRICAL_SURFACE ( 'NONE', #11498, 8.099999999999999645 ) ;
#15442=EDGE_CURVE ( 'NONE', #16873, #3875, #17562, .T. ) ;
#15455=LINE ( 'NONE', #2405, #13600 ) ;
#15504=EDGE_LOOP ( 'NONE', ( #16385, #14606 ) ) ;
#15514=EDGE_LOOP ( 'NONE', ( #287, #10911, #5655, #12315 ) ) ;
#15595=LINE ( 'NONE', #8628, #18279 ) ;
#15631=DIRECTION ( 'NONE',  ( 1.000000000000000000, 0.000000000000000000, 0.000000000000000000 ) ) ;
#15649=VERTEX_POINT ( 'NONE', #1642 ) ;
#15732=CIRCLE ( 'NONE', #10243, 4.799999999999999822 ) ;
#15779=DIRECTION ( 'NONE',  ( 0.000000000000000000, 0.000000000000000000, 1.000000000000000000 ) ) ;
#15845=FACE_OUTER_BOUND ( 'NONE', #8285, .T. ) ;
#15865=DIRECTION ( 'NONE',  ( 1.000000000000000000, 0.000000000000000000, 0.000000000000000000 ) ) ;
#15882=EDGE_CURVE ( 'NONE', #17177, #16873, #18686, .T. ) ;
#15905=LINE ( 'NONE', #7131, #2077 ) ;
#15914=CARTESIAN_POINT ( 'NONE',  ( 0.000000000000000000, 0.000000000000000000, -1.000000000000000000 ) ) ;
#15925=CARTESIAN_POINT ( 'NONE',  ( 6.080745460913608902, 0.5192545390863916310, 0.000000000000000000 ) ) ;
#15969=PLANE ( 'NONE',  #8891 ) ;
#15974=VERTEX_POINT ( 'NONE', #16484 ) ;
#15989=FACE_OUTER_BOUND ( 'NONE', #10123, .T. ) ;
#15997=CARTESIAN_POINT ( 'NONE',  ( -4.799999999999999822, 5.878304635907294211E-16, -1.000000000000000000 ) ) ;
#16085=AXIS2_PLACEMENT_3D ( 'NONE', #9748, #9929, #17092 ) ;
#16134=CIRCLE ( 'NONE', #8241, 6.080745460913608902 ) ;
#16232=ORIENTED_EDGE ( 'NONE', *, *, #17782, .T. ) ;
#16282=VECTOR ( 'NONE', #8320, 1000.000000000000000 ) ;
#16295=DIRECTION ( 'NONE',  ( 1.000000000000000000, 0.000000000000000000, 0.000000000000000000 ) ) ;
#16360=SURFACE_SIDE_STYLE ('',( #15022 ) ) ;
#16385=ORIENTED_EDGE ( 'NONE', *, *, #5629, .F. ) ;
#16417=CARTESIAN_POINT ( 'NONE',  ( 6.080745460913608902, 0.5192545390863916310, -1.000000000000000000 ) ) ;
#16434=AXIS2_PLACEMENT_3D ( 'NONE', #10052, #11668, #15865 ) ;
#16449=ORIENTED_EDGE ( 'NONE', *, *, #686, .T. ) ;
#16473=EDGE_CURVE ( 'NONE', #276, #15649, #13611, .T. ) ;
#16484=CARTESIAN_POINT ( 'NONE',  ( -6.080745460913608902, 0.5192545390863924082, 0.000000000000000000 ) ) ;
#16548=DIRECTION ( 'NONE',  ( 0.000000000000000000, 0.000000000000000000, 1.000000000000000000 ) ) ;
#16584=ORIENTED_EDGE ( 'NONE', *, *, #12858, .F. ) ;
#16600=DIRECTION ( 'NONE',  ( 0.000000000000000000, 0.000000000000000000, 1.000000000000000000 ) ) ;
#16604=CYLINDRICAL_SURFACE ( 'NONE', #9530, 4.799999999999999822 ) ;
#16631=VERTEX_POINT ( 'NONE', #12840 ) ;
#16638=AXIS2_PLACEMENT_3D ( 'NONE', #5908, #742, #7526 ) ;
#16646=VECTOR ( 'NONE', #13757, 1000.000000000000000 ) ;
#16708=DIRECTION ( 'NONE',  ( 0.9914448613738102711, -0.1305261922200524338, 0.000000000000000000 ) ) ;
#16710=DIRECTION ( 'NONE',  ( 0.000000000000000000, 0.000000000000000000, 1.000000000000000000 ) ) ;
#16714=CARTESIAN_POINT ( 'NONE',  ( -2.595115354961444076, -7.673029147243174641, -1.000000000000000000 ) ) ;
#16734=DIRECTION ( 'NONE',  ( -0.000000000000000000, -0.000000000000000000, -1.000000000000000000 ) ) ;
#16780=CARTESIAN_POINT ( 'NONE',  ( -2.595115354961444076, -7.673029147243174641, 0.000000000000000000 ) ) ;
#16792=DIRECTION ( 'NONE',  ( 1.000000000000000000, 0.000000000000000000, 0.000000000000000000 ) ) ;
#16824=CARTESIAN_POINT ( 'NONE',  ( 0.000000000000000000, 0.000000000000000000, 0.000000000000000000 ) ) ;
#16864=DIRECTION ( 'NONE',  ( 0.000000000000000000, 0.000000000000000000, 1.000000000000000000 ) ) ;
#16873=VERTEX_POINT ( 'NONE', #18116 ) ;
#16883=DIRECTION ( 'NONE',  ( 1.000000000000000000, 0.000000000000000000, 0.000000000000000000 ) ) ;
#16981=ORIENTED_EDGE ( 'NONE', *, *, #7942, .T. ) ;
#16998=ORIENTED_EDGE ( 'NONE', *, *, #8194, .F. ) ;
#17009=VERTEX_POINT ( 'NONE', #7344 ) ;
#17048=( GEOMETRIC_REPRESENTATION_CONTEXT ( 3 ) GLOBAL_UNCERTAINTY_ASSIGNED_CONTEXT ( ( #2150 ) ) GLOBAL_UNIT_ASSIGNED_CONTEXT ( ( #3560, #15181, #9450 ) ) REPRESENTATION_CONTEXT ( 'NONE', 'WORKASPACE' ) );
#17068=EDGE_CURVE ( 'NONE', #2784, #6911, #4225, .T. ) ;
#17092=DIRECTION ( 'NONE',  ( 1.000000000000000000, 0.000000000000000000, 0.000000000000000000 ) ) ;
#17100=DIRECTION ( 'NONE',  ( 1.000000000000000000, 0.000000000000000000, 0.000000000000000000 ) ) ;
#17101=ORIENTED_EDGE ( 'NONE', *, *, #7942, .F. ) ;
#17135=ORIENTED_EDGE ( 'NONE', *, *, #12500, .T. ) ;
#17152=DIRECTION ( 'NONE',  ( -0.000000000000000000, -0.000000000000000000, -1.000000000000000000 ) ) ;
#17177=VERTEX_POINT ( 'NONE', #13252 ) ;
#17277=CARTESIAN_POINT ( 'NONE',  ( 2.000000000000000000, -6.429618962271402616, -1.000000000000000000 ) ) ;
#17297=DIRECTION ( 'NONE',  ( 0.03086419753086420623, -0.9995235871707959241, 0.000000000000000000 ) ) ;
#17313=ORIENTED_EDGE ( 'NONE', *, *, #14704, .T. ) ;
#17339=STYLED_ITEM('',(#18876),#9242);
#17343=DIRECTION ( 'NONE',  ( 1.000000000000000000, 0.000000000000000000, 0.000000000000000000 ) ) ;
#17351=EDGE_LOOP ( 'NONE', ( #15048, #11365, #13473, #18154 ) ) ;
#17397=EDGE_CURVE ( 'NONE', #7573, #7040, #5235, .T. ) ;
#17433=CLOSED_SHELL ( 'NONE', ( #17742, #13198, #6402, #4875, #8291, #18471, #15073, #17942, #14713, #9918, #2030, #7782, #5298, #4343, #12258, #2851, #5621, #13199, #17826, #7594, #6620, #6506 ) ) ;
#17489=CARTESIAN_POINT ( 'NONE',  ( -1.250000000000000000, -6.429618962271402616, 0.000000000000000000 ) ) ;
#17490=VECTOR ( 'NONE', #4695, 1000.000000000000000 ) ;
#17497=EDGE_LOOP ( 'NONE', ( #1834, #10923, #14575, #17135 ) ) ;
#17512=DIRECTION ( 'NONE',  ( 1.000000000000000000, 0.000000000000000000, 0.000000000000000000 ) ) ;
#17545=CARTESIAN_POINT ( 'NONE',  ( 0.000000000000000000, 0.5192545390863916310, -1.000000000000000000 ) ) ;
#17559=DIRECTION ( 'NONE',  ( 0.1305261922200524616, 0.9914448613738103822, -0.000000000000000000 ) ) ;
#17562=LINE ( 'NONE', #4328, #2682 ) ;
#17576=CARTESIAN_POINT ( 'NONE',  ( 3.309651814758564736, -5.455921364805393026, -1.000000000000000000 ) ) ;
#17586=CIRCLE ( 'NONE', #9372, 4.799999999999999822 ) ;
#17606=AXIS2_PLACEMENT_3D ( 'NONE', #3357, #9151, #4588 ) ;
#17630=ORIENTED_EDGE ( 'NONE', *, *, #12136, .T. ) ;
#17642=DIRECTION ( 'NONE',  ( 0.000000000000000000, 0.000000000000000000, 1.000000000000000000 ) ) ;
#17682=VERTEX_POINT ( 'NONE', #9309 ) ;
#17684=FACE_OUTER_BOUND ( 'NONE', #4718, .T. ) ;
#17742=ADVANCED_FACE ( 'NONE', ( #13617 ), #17987, .F. ) ;
#17761=DIRECTION ( 'NONE',  ( 1.000000000000000000, 0.000000000000000000, 0.000000000000000000 ) ) ;
#17782=EDGE_CURVE ( 'NONE', #9002, #14729, #15286, .T. ) ;
#17784=CARTESIAN_POINT ( 'NONE',  ( 1.250000000000000000, -6.429618962271402616, -1.000000000000000000 ) ) ;
#17826=ADVANCED_FACE ( 'NONE', ( #12554, #5601, #6941 ), #5422, .F. ) ;
#17844=DIRECTION ( 'NONE',  ( 0.000000000000000000, 0.000000000000000000, 1.000000000000000000 ) ) ;
#17916=CARTESIAN_POINT ( 'NONE',  ( -4.799999999999999822, 5.878304635907294211E-16, 0.000000000000000000 ) ) ;
#17920=DIRECTION ( 'NONE',  ( 0.000000000000000000, 0.000000000000000000, 1.000000000000000000 ) ) ;
#17942=ADVANCED_FACE ( 'NONE', ( #17684 ), #15969, .T. ) ;
#17957=CARTESIAN_POINT ( 'NONE',  ( -5.686050877451574337, -5.768780236673276995, -1.000000000000000000 ) ) ;
#17972=ORIENTED_EDGE ( 'NONE', *, *, #15442, .F. ) ;
#17986=CARTESIAN_POINT ( 'NONE',  ( 0.000000000000000000, 0.5192545390863916310, 0.000000000000000000 ) ) ;
#17987=CYLINDRICAL_SURFACE ( 'NONE', #7676, 0.7500000000000000000 ) ;
#18003=CARTESIAN_POINT ( 'NONE',  ( -3.309651814758565180, -5.455921364805393026, -1.000000000000000000 ) ) ;
#18018=DIRECTION ( 'NONE',  ( 1.000000000000000000, 0.000000000000000000, 0.000000000000000000 ) ) ;
#18056=( LENGTH_UNIT ( ) NAMED_UNIT ( * ) SI_UNIT ( .MILLI., .METRE. ) );
#18065=COLOUR_RGB ( '',1.000000000000000000, 0.9490196078431372140, 0.9098039215686274384 ) ;
#18070=DIRECTION ( 'NONE',  ( 1.000000000000000000, 0.000000000000000000, 0.000000000000000000 ) ) ;
#18116=CARTESIAN_POINT ( 'NONE',  ( 0.1481481481481481122, -4.797713218419819903, 0.000000000000000000 ) ) ;
#18117=VECTOR ( 'NONE', #15779, 1000.000000000000000 ) ;
#18124=PLANE ( 'NONE',  #11502 ) ;
#18154=ORIENTED_EDGE ( 'NONE', *, *, #4305, .T. ) ;
#18198=EDGE_LOOP ( 'NONE', ( #17972, #1582, #15254, #1049 ) ) ;
#18208=VECTOR ( 'NONE', #2487, 1000.000000000000114 ) ;
#18220=CIRCLE ( 'NONE', #10015, 8.099999999999999645 ) ;
#18232=CARTESIAN_POINT ( 'NONE',  ( 4.078421086530217288, -3.990950201428958621, 0.000000000000000000 ) ) ;
#18255=ORIENTED_EDGE ( 'NONE', *, *, #14388, .T. ) ;
#18262=VECTOR ( 'NONE', #17559, 999.9999999999998863 ) ;
#18275=EDGE_CURVE ( 'NONE', #6911, #2085, #12882, .T. ) ;
#18279=VECTOR ( 'NONE', #9971, 1000.000000000000000 ) ;
#18345=CARTESIAN_POINT ( 'NONE',  ( 0.000000000000000000, 0.000000000000000000, 0.000000000000000000 ) ) ;
#18375=DIRECTION ( 'NONE',  ( 1.000000000000000000, 0.000000000000000000, 0.000000000000000000 ) ) ;
#18384=ORIENTED_EDGE ( 'NONE', *, *, #5629, .T. ) ;
#18406=CARTESIAN_POINT ( 'NONE',  ( -3.098410542199071749, -7.060458129626440815, -1.000000000000000000 ) ) ;
#18471=ADVANCED_FACE ( 'NONE', ( #9264 ), #16604, .F. ) ;
#18482=AXIS2_PLACEMENT_3D ( 'NONE', #17489, #5788, #13207 ) ;
#18565=DIRECTION ( 'NONE',  ( 1.000000000000000000, 0.000000000000000000, 0.000000000000000000 ) ) ;
#18624=CARTESIAN_POINT ( 'NONE',  ( 0.2499999999999966416, -8.096141056083448362, -1.000000000000000000 ) ) ;
#18628=FACE_OUTER_BOUND ( 'NONE', #2005, .T. ) ;
#18632=PRODUCT_DEFINITION_SHAPE ( 'NONE', 'NONE',  #8300 ) ;
#18686=LINE ( 'NONE', #5825, #12423 ) ;
#18724=AXIS2_PLACEMENT_3D ( 'NONE', #4167, #152, #11677 ) ;
#18726=CIRCLE ( 'NONE', #176, 0.7500000000000000000 ) ;
#18729=VERTEX_POINT ( 'NONE', #16714 ) ;
#18739=VECTOR ( 'NONE', #17844, 1000.000000000000000 ) ;
#18740=EDGE_CURVE ( 'NONE', #17177, #7394, #2419, .T. ) ;
#18802=ORIENTED_EDGE ( 'NONE', *, *, #10109, .F. ) ;
#18870=COLOUR_RGB('Grey',0.48,0.52,0.57);
#18871=FILL_AREA_STYLE_COLOUR('',#18870);
#18872=FILL_AREA_STYLE('',(#18871));
#18873=SURFACE_STYLE_FILL_AREA(#18872);
#18874=SURFACE_SIDE_STYLE('',(#18873));
#18875=SURFACE_STYLE_USAGE(.BOTH.,#18874);
#18876=PRESENTATION_STYLE_ASSIGNMENT((#18875));
ENDSEC;
END-ISO-10303-21;
